ISO-10303-21;
HEADER;
/* Generated by software containing ST-Developer
 * from STEP Tools, Inc. (www.steptools.com) 
 */

FILE_DESCRIPTION(
/* description */ ('PAT-072'),
/* implementation_level */ '2;1');

FILE_NAME(
/* name */ 'Cap Screw - M4x16.step',
/* time_stamp */ '2026-10-29T20:11:56-07:00',
/* author */ (''),
/* organization */ (''),
/* preprocessor_version */ 'ST-DEVELOPER v20.2',
/* originating_system */ 'Autodesk Translation Framework v15.17.0.0',
/* authorisation */ '');

FILE_SCHEMA (('AUTOMOTIVE_DESIGN { 1 0 10303 214 3 1 1 }'));
ENDSEC;

DATA;
#10=MECHANICAL_DESIGN_GEOMETRIC_PRESENTATION_REPRESENTATION('',(#367),#11432);
#216=CONICAL_SURFACE('',#7188,0.325,0.785398163397448);
#217=CONICAL_SURFACE('',#7192,0.335,0.785398163397448);
#218=CONICAL_SURFACE('',#7196,0.21,0.463647609000806);
#219=CONICAL_SURFACE('',#7200,0.18,0.785398163397448);
#221=ORIENTED_CLOSED_SHELL('',*,#6104,.F.);
#223=BREP_WITH_VOIDS('Body1',#6103,(#221));
#295=SHAPE_REPRESENTATION_RELATIONSHIP('SRR','None',#11600,#331);
#331=ADVANCED_BREP_SHAPE_REPRESENTATION('',(#223),#11431);
#367=STYLED_ITEM('',(#11826),#223);
#569=FACE_BOUND('',#1695,.T.);
#785=PLANE('',#7186);
#786=PLANE('',#7194);
#787=PLANE('',#7202);
#788=PLANE('',#7203);
#789=PLANE('',#7204);
#790=PLANE('',#7205);
#791=PLANE('',#7206);
#792=PLANE('',#7207);
#793=PLANE('',#7208);
#794=PLANE('',#7209);
#795=PLANE('',#7210);
#1151=FACE_OUTER_BOUND('',#1690,.T.);
#1152=FACE_OUTER_BOUND('',#1691,.T.);
#1153=FACE_OUTER_BOUND('',#1692,.T.);
#1154=FACE_OUTER_BOUND('',#1693,.T.);
#1155=FACE_OUTER_BOUND('',#1694,.T.);
#1156=FACE_OUTER_BOUND('',#1696,.T.);
#1157=FACE_OUTER_BOUND('',#1697,.T.);
#1158=FACE_OUTER_BOUND('',#1698,.T.);
#1159=FACE_OUTER_BOUND('',#1699,.T.);
#1160=FACE_OUTER_BOUND('',#1700,.T.);
#1161=FACE_OUTER_BOUND('',#1701,.T.);
#1162=FACE_OUTER_BOUND('',#1702,.T.);
#1163=FACE_OUTER_BOUND('',#1703,.T.);
#1164=FACE_OUTER_BOUND('',#1704,.T.);
#1165=FACE_OUTER_BOUND('',#1705,.T.);
#1166=FACE_OUTER_BOUND('',#1706,.T.);
#1167=FACE_OUTER_BOUND('',#1707,.T.);
#1690=EDGE_LOOP('',(#5494));
#1691=EDGE_LOOP('',(#5495,#5496,#5497,#5498));
#1692=EDGE_LOOP('',(#5499,#5500,#5501,#5502));
#1693=EDGE_LOOP('',(#5503,#5504,#5505,#5506));
#1694=EDGE_LOOP('',(#5507));
#1695=EDGE_LOOP('',(#5508));
#1696=EDGE_LOOP('',(#5509,#5510,#5511,#5512));
#1697=EDGE_LOOP('',(#5513,#5514,#5515,#5516));
#1698=EDGE_LOOP('',(#5517,#5518,#5519,#5520));
#1699=EDGE_LOOP('',(#5521));
#1700=EDGE_LOOP('',(#5522,#5523,#5524,#5525));
#1701=EDGE_LOOP('',(#5526,#5527,#5528,#5529));
#1702=EDGE_LOOP('',(#5530,#5531,#5532,#5533));
#1703=EDGE_LOOP('',(#5534,#5535,#5536,#5537));
#1704=EDGE_LOOP('',(#5538,#5539,#5540,#5541));
#1705=EDGE_LOOP('',(#5542,#5543,#5544,#5545));
#1706=EDGE_LOOP('',(#5546,#5547,#5548,#5549,#5550,#5551));
#1707=EDGE_LOOP('',(#5552,#5553,#5554,#5555,#5556,#5557));
#2103=LINE('',#11244,#2522);
#2104=LINE('',#11248,#2523);
#2105=LINE('',#11252,#2524);
#2106=LINE('',#11259,#2525);
#2107=LINE('',#11263,#2526);
#2108=LINE('',#11267,#2527);
#2109=LINE('',#11272,#2528);
#2110=LINE('',#11274,#2529);
#2111=LINE('',#11276,#2530);
#2112=LINE('',#11277,#2531);
#2113=LINE('',#11280,#2532);
#2114=LINE('',#11282,#2533);
#2115=LINE('',#11283,#2534);
#2116=LINE('',#11286,#2535);
#2117=LINE('',#11288,#2536);
#2118=LINE('',#11289,#2537);
#2119=LINE('',#11292,#2538);
#2120=LINE('',#11294,#2539);
#2121=LINE('',#11295,#2540);
#2122=LINE('',#11298,#2541);
#2123=LINE('',#11300,#2542);
#2124=LINE('',#11301,#2543);
#2125=LINE('',#11303,#2544);
#2126=LINE('',#11304,#2545);
#2522=VECTOR('',#9030,0.325);
#2523=VECTOR('',#9035,0.35);
#2524=VECTOR('',#9040,0.335);
#2525=VECTOR('',#9049,0.21);
#2526=VECTOR('',#9054,0.2);
#2527=VECTOR('',#9059,0.18);
#2528=VECTOR('',#9064,1.);
#2529=VECTOR('',#9065,1.);
#2530=VECTOR('',#9066,1.);
#2531=VECTOR('',#9067,1.);
#2532=VECTOR('',#9070,1.);
#2533=VECTOR('',#9071,1.);
#2534=VECTOR('',#9072,1.);
#2535=VECTOR('',#9075,1.);
#2536=VECTOR('',#9076,1.);
#2537=VECTOR('',#9077,1.);
#2538=VECTOR('',#9080,1.);
#2539=VECTOR('',#9081,1.);
#2540=VECTOR('',#9082,1.);
#2541=VECTOR('',#9085,1.);
#2542=VECTOR('',#9086,1.);
#2543=VECTOR('',#9087,1.);
#2544=VECTOR('',#9090,1.);
#2545=VECTOR('',#9091,1.);
#2828=CIRCLE('',#7187,0.3);
#2829=CIRCLE('',#7189,0.35);
#2830=CIRCLE('',#7191,0.35);
#2831=CIRCLE('',#7193,0.32);
#2832=CIRCLE('',#7195,0.22);
#2833=CIRCLE('',#7197,0.1954);
#2834=CIRCLE('',#7199,0.1954);
#2835=CIRCLE('',#7201,0.16);
#3303=VERTEX_POINT('',#11239);
#3304=VERTEX_POINT('',#11242);
#3305=VERTEX_POINT('',#11246);
#3306=VERTEX_POINT('',#11250);
#3307=VERTEX_POINT('',#11254);
#3308=VERTEX_POINT('',#11257);
#3309=VERTEX_POINT('',#11261);
#3310=VERTEX_POINT('',#11265);
#3311=VERTEX_POINT('',#11270);
#3312=VERTEX_POINT('',#11271);
#3313=VERTEX_POINT('',#11273);
#3314=VERTEX_POINT('',#11275);
#3315=VERTEX_POINT('',#11279);
#3316=VERTEX_POINT('',#11281);
#3317=VERTEX_POINT('',#11285);
#3318=VERTEX_POINT('',#11287);
#3319=VERTEX_POINT('',#11291);
#3320=VERTEX_POINT('',#11293);
#3321=VERTEX_POINT('',#11297);
#3322=VERTEX_POINT('',#11299);
#4036=EDGE_CURVE('',#3303,#3303,#2828,.T.);
#4037=EDGE_CURVE('',#3304,#3304,#2829,.T.);
#4038=EDGE_CURVE('',#3304,#3303,#2103,.T.);
#4039=EDGE_CURVE('',#3305,#3305,#2830,.T.);
#4040=EDGE_CURVE('',#3305,#3304,#2104,.T.);
#4041=EDGE_CURVE('',#3306,#3306,#2831,.T.);
#4042=EDGE_CURVE('',#3306,#3305,#2105,.T.);
#4043=EDGE_CURVE('',#3307,#3307,#2832,.T.);
#4044=EDGE_CURVE('',#3308,#3308,#2833,.F.);
#4045=EDGE_CURVE('',#3308,#3307,#2106,.T.);
#4046=EDGE_CURVE('',#3309,#3309,#2834,.F.);
#4047=EDGE_CURVE('',#3309,#3308,#2107,.T.);
#4048=EDGE_CURVE('',#3310,#3310,#2835,.T.);
#4049=EDGE_CURVE('',#3310,#3309,#2108,.T.);
#4050=EDGE_CURVE('',#3311,#3312,#2109,.T.);
#4051=EDGE_CURVE('',#3312,#3313,#2110,.T.);
#4052=EDGE_CURVE('',#3313,#3314,#2111,.T.);
#4053=EDGE_CURVE('',#3311,#3314,#2112,.T.);
#4054=EDGE_CURVE('',#3312,#3315,#2113,.T.);
#4055=EDGE_CURVE('',#3315,#3316,#2114,.T.);
#4056=EDGE_CURVE('',#3316,#3313,#2115,.T.);
#4057=EDGE_CURVE('',#3315,#3317,#2116,.T.);
#4058=EDGE_CURVE('',#3317,#3318,#2117,.T.);
#4059=EDGE_CURVE('',#3318,#3316,#2118,.T.);
#4060=EDGE_CURVE('',#3317,#3319,#2119,.T.);
#4061=EDGE_CURVE('',#3319,#3320,#2120,.T.);
#4062=EDGE_CURVE('',#3320,#3318,#2121,.T.);
#4063=EDGE_CURVE('',#3319,#3321,#2122,.T.);
#4064=EDGE_CURVE('',#3321,#3322,#2123,.T.);
#4065=EDGE_CURVE('',#3322,#3320,#2124,.T.);
#4066=EDGE_CURVE('',#3321,#3311,#2125,.T.);
#4067=EDGE_CURVE('',#3314,#3322,#2126,.T.);
#5494=ORIENTED_EDGE('',*,*,#4036,.F.);
#5495=ORIENTED_EDGE('',*,*,#4037,.F.);
#5496=ORIENTED_EDGE('',*,*,#4038,.T.);
#5497=ORIENTED_EDGE('',*,*,#4036,.T.);
#5498=ORIENTED_EDGE('',*,*,#4038,.F.);
#5499=ORIENTED_EDGE('',*,*,#4039,.F.);
#5500=ORIENTED_EDGE('',*,*,#4040,.T.);
#5501=ORIENTED_EDGE('',*,*,#4037,.T.);
#5502=ORIENTED_EDGE('',*,*,#4040,.F.);
#5503=ORIENTED_EDGE('',*,*,#4041,.F.);
#5504=ORIENTED_EDGE('',*,*,#4042,.T.);
#5505=ORIENTED_EDGE('',*,*,#4039,.T.);
#5506=ORIENTED_EDGE('',*,*,#4042,.F.);
#5507=ORIENTED_EDGE('',*,*,#4041,.T.);
#5508=ORIENTED_EDGE('',*,*,#4043,.F.);
#5509=ORIENTED_EDGE('',*,*,#4044,.F.);
#5510=ORIENTED_EDGE('',*,*,#4045,.T.);
#5511=ORIENTED_EDGE('',*,*,#4043,.T.);
#5512=ORIENTED_EDGE('',*,*,#4045,.F.);
#5513=ORIENTED_EDGE('',*,*,#4046,.F.);
#5514=ORIENTED_EDGE('',*,*,#4047,.T.);
#5515=ORIENTED_EDGE('',*,*,#4044,.T.);
#5516=ORIENTED_EDGE('',*,*,#4047,.F.);
#5517=ORIENTED_EDGE('',*,*,#4048,.F.);
#5518=ORIENTED_EDGE('',*,*,#4049,.T.);
#5519=ORIENTED_EDGE('',*,*,#4046,.T.);
#5520=ORIENTED_EDGE('',*,*,#4049,.F.);
#5521=ORIENTED_EDGE('',*,*,#4048,.T.);
#5522=ORIENTED_EDGE('',*,*,#4050,.T.);
#5523=ORIENTED_EDGE('',*,*,#4051,.T.);
#5524=ORIENTED_EDGE('',*,*,#4052,.T.);
#5525=ORIENTED_EDGE('',*,*,#4053,.F.);
#5526=ORIENTED_EDGE('',*,*,#4054,.T.);
#5527=ORIENTED_EDGE('',*,*,#4055,.T.);
#5528=ORIENTED_EDGE('',*,*,#4056,.T.);
#5529=ORIENTED_EDGE('',*,*,#4051,.F.);
#5530=ORIENTED_EDGE('',*,*,#4057,.T.);
#5531=ORIENTED_EDGE('',*,*,#4058,.T.);
#5532=ORIENTED_EDGE('',*,*,#4059,.T.);
#5533=ORIENTED_EDGE('',*,*,#4055,.F.);
#5534=ORIENTED_EDGE('',*,*,#4060,.T.);
#5535=ORIENTED_EDGE('',*,*,#4061,.T.);
#5536=ORIENTED_EDGE('',*,*,#4062,.T.);
#5537=ORIENTED_EDGE('',*,*,#4058,.F.);
#5538=ORIENTED_EDGE('',*,*,#4063,.T.);
#5539=ORIENTED_EDGE('',*,*,#4064,.T.);
#5540=ORIENTED_EDGE('',*,*,#4065,.T.);
#5541=ORIENTED_EDGE('',*,*,#4061,.F.);
#5542=ORIENTED_EDGE('',*,*,#4066,.T.);
#5543=ORIENTED_EDGE('',*,*,#4053,.T.);
#5544=ORIENTED_EDGE('',*,*,#4067,.T.);
#5545=ORIENTED_EDGE('',*,*,#4064,.F.);
#5546=ORIENTED_EDGE('',*,*,#4066,.F.);
#5547=ORIENTED_EDGE('',*,*,#4063,.F.);
#5548=ORIENTED_EDGE('',*,*,#4060,.F.);
#5549=ORIENTED_EDGE('',*,*,#4057,.F.);
#5550=ORIENTED_EDGE('',*,*,#4054,.F.);
#5551=ORIENTED_EDGE('',*,*,#4050,.F.);
#5552=ORIENTED_EDGE('',*,*,#4067,.F.);
#5553=ORIENTED_EDGE('',*,*,#4052,.F.);
#5554=ORIENTED_EDGE('',*,*,#4056,.F.);
#5555=ORIENTED_EDGE('',*,*,#4059,.F.);
#5556=ORIENTED_EDGE('',*,*,#4062,.F.);
#5557=ORIENTED_EDGE('',*,*,#4065,.F.);
#5693=CYLINDRICAL_SURFACE('',#7190,0.35);
#5694=CYLINDRICAL_SURFACE('',#7198,0.1954);
#6050=ADVANCED_FACE('',(#1151),#785,.T.);
#6051=ADVANCED_FACE('',(#1152),#216,.T.);
#6052=ADVANCED_FACE('',(#1153),#5693,.T.);
#6053=ADVANCED_FACE('',(#1154),#217,.T.);
#6054=ADVANCED_FACE('',(#1155,#569),#786,.T.);
#6055=ADVANCED_FACE('',(#1156),#218,.T.);
#6056=ADVANCED_FACE('',(#1157),#5694,.T.);
#6057=ADVANCED_FACE('',(#1158),#219,.T.);
#6058=ADVANCED_FACE('',(#1159),#787,.T.);
#6059=ADVANCED_FACE('',(#1160),#788,.F.);
#6060=ADVANCED_FACE('',(#1161),#789,.F.);
#6061=ADVANCED_FACE('',(#1162),#790,.F.);
#6062=ADVANCED_FACE('',(#1163),#791,.F.);
#6063=ADVANCED_FACE('',(#1164),#792,.F.);
#6064=ADVANCED_FACE('',(#1165),#793,.F.);
#6065=ADVANCED_FACE('',(#1166),#794,.F.);
#6066=ADVANCED_FACE('',(#1167),#795,.F.);
#6103=CLOSED_SHELL('',(#6050,#6051,#6052,#6053,#6054,#6055,#6056,#6057,
#6058));
#6104=CLOSED_SHELL('',(#6059,#6060,#6061,#6062,#6063,#6064,#6065,#6066));
#7185=AXIS2_PLACEMENT_3D('',#11237,#9020,#9021);
#7186=AXIS2_PLACEMENT_3D('',#11238,#9022,#9023);
#7187=AXIS2_PLACEMENT_3D('',#11240,#9024,#9025);
#7188=AXIS2_PLACEMENT_3D('',#11241,#9026,#9027);
#7189=AXIS2_PLACEMENT_3D('',#11243,#9028,#9029);
#7190=AXIS2_PLACEMENT_3D('',#11245,#9031,#9032);
#7191=AXIS2_PLACEMENT_3D('',#11247,#9033,#9034);
#7192=AXIS2_PLACEMENT_3D('',#11249,#9036,#9037);
#7193=AXIS2_PLACEMENT_3D('',#11251,#9038,#9039);
#7194=AXIS2_PLACEMENT_3D('',#11253,#9041,#9042);
#7195=AXIS2_PLACEMENT_3D('',#11255,#9043,#9044);
#7196=AXIS2_PLACEMENT_3D('',#11256,#9045,#9046);
#7197=AXIS2_PLACEMENT_3D('',#11258,#9047,#9048);
#7198=AXIS2_PLACEMENT_3D('',#11260,#9050,#9051);
#7199=AXIS2_PLACEMENT_3D('',#11262,#9052,#9053);
#7200=AXIS2_PLACEMENT_3D('',#11264,#9055,#9056);
#7201=AXIS2_PLACEMENT_3D('',#11266,#9057,#9058);
#7202=AXIS2_PLACEMENT_3D('',#11268,#9060,#9061);
#7203=AXIS2_PLACEMENT_3D('',#11269,#9062,#9063);
#7204=AXIS2_PLACEMENT_3D('',#11278,#9068,#9069);
#7205=AXIS2_PLACEMENT_3D('',#11284,#9073,#9074);
#7206=AXIS2_PLACEMENT_3D('',#11290,#9078,#9079);
#7207=AXIS2_PLACEMENT_3D('',#11296,#9083,#9084);
#7208=AXIS2_PLACEMENT_3D('',#11302,#9088,#9089);
#7209=AXIS2_PLACEMENT_3D('',#11305,#9092,#9093);
#7210=AXIS2_PLACEMENT_3D('',#11306,#9094,#9095);
#9020=DIRECTION('axis',(0.,0.,1.));
#9021=DIRECTION('refdir',(1.,0.,0.));
#9022=DIRECTION('center_axis',(0.,1.,0.));
#9023=DIRECTION('ref_axis',(0.,0.,1.));
#9024=DIRECTION('center_axis',(0.,-1.,0.));
#9025=DIRECTION('ref_axis',(1.,0.,0.));
#9026=DIRECTION('center_axis',(0.,-1.,0.));
#9027=DIRECTION('ref_axis',(1.,0.,0.));
#9028=DIRECTION('center_axis',(0.,-1.,0.));
#9029=DIRECTION('ref_axis',(1.,0.,0.));
#9030=DIRECTION('',(0.707106781186547,0.707106781186548,8.65956056235493E-17));
#9031=DIRECTION('center_axis',(0.,-1.,0.));
#9032=DIRECTION('ref_axis',(1.,0.,0.));
#9033=DIRECTION('center_axis',(0.,-1.,0.));
#9034=DIRECTION('ref_axis',(1.,0.,0.));
#9035=DIRECTION('',(0.,1.,0.));
#9036=DIRECTION('center_axis',(0.,1.,0.));
#9037=DIRECTION('ref_axis',(1.,0.,0.));
#9038=DIRECTION('center_axis',(0.,-1.,0.));
#9039=DIRECTION('ref_axis',(1.,0.,0.));
#9040=DIRECTION('',(-0.707106781186547,0.707106781186548,-8.65956056235493E-17));
#9041=DIRECTION('center_axis',(0.,-1.,0.));
#9042=DIRECTION('ref_axis',(0.,0.,-1.));
#9043=DIRECTION('center_axis',(0.,-1.,0.));
#9044=DIRECTION('ref_axis',(1.,0.,0.));
#9045=DIRECTION('center_axis',(0.,1.,0.));
#9046=DIRECTION('ref_axis',(1.,0.,0.));
#9047=DIRECTION('center_axis',(0.,1.,0.));
#9048=DIRECTION('ref_axis',(1.,0.,0.));
#9049=DIRECTION('',(-0.447213595499958,0.894427190999916,-5.47678698264203E-17));
#9050=DIRECTION('center_axis',(0.,-1.,0.));
#9051=DIRECTION('ref_axis',(1.,0.,0.));
#9052=DIRECTION('center_axis',(0.,1.,0.));
#9053=DIRECTION('ref_axis',(1.,0.,0.));
#9054=DIRECTION('',(0.,1.,0.));
#9055=DIRECTION('center_axis',(0.,1.,0.));
#9056=DIRECTION('ref_axis',(1.,0.,0.));
#9057=DIRECTION('center_axis',(0.,-1.,0.));
#9058=DIRECTION('ref_axis',(1.,0.,0.));
#9059=DIRECTION('',(-0.707106781186547,0.707106781186548,-8.65956056235493E-17));
#9060=DIRECTION('center_axis',(0.,-1.,0.));
#9061=DIRECTION('ref_axis',(0.,0.,-1.));
#9062=DIRECTION('center_axis',(0.866025403784439,0.,-0.5));
#9063=DIRECTION('ref_axis',(0.5,0.,0.866025403784439));
#9064=DIRECTION('',(-0.5,0.,-0.866025403784439));
#9065=DIRECTION('',(0.,-1.,0.));
#9066=DIRECTION('',(0.5,0.,0.866025403784439));
#9067=DIRECTION('',(0.,-1.,0.));
#9068=DIRECTION('center_axis',(1.60246890531964E-16,0.,-1.));
#9069=DIRECTION('ref_axis',(1.,0.,1.60246890531964E-16));
#9070=DIRECTION('',(-1.,0.,-1.60246890531964E-16));
#9071=DIRECTION('',(0.,-1.,0.));
#9072=DIRECTION('',(1.,0.,1.60246890531964E-16));
#9073=DIRECTION('center_axis',(-0.866025403784439,0.,-0.5));
#9074=DIRECTION('ref_axis',(0.5,0.,-0.866025403784439));
#9075=DIRECTION('',(-0.5,0.,0.866025403784439));
#9076=DIRECTION('',(0.,-1.,0.));
#9077=DIRECTION('',(0.5,0.,-0.866025403784439));
#9078=DIRECTION('center_axis',(-0.866025403784439,0.,0.5));
#9079=DIRECTION('ref_axis',(-0.5,0.,-0.866025403784439));
#9080=DIRECTION('',(0.5,0.,0.866025403784439));
#9081=DIRECTION('',(0.,-1.,0.));
#9082=DIRECTION('',(-0.5,0.,-0.866025403784439));
#9083=DIRECTION('center_axis',(-1.60246890531964E-16,0.,1.));
#9084=DIRECTION('ref_axis',(-1.,0.,-1.60246890531964E-16));
#9085=DIRECTION('',(1.,0.,1.60246890531964E-16));
#9086=DIRECTION('',(0.,-1.,0.));
#9087=DIRECTION('',(-1.,0.,-1.60246890531964E-16));
#9088=DIRECTION('center_axis',(0.866025403784439,0.,0.5));
#9089=DIRECTION('ref_axis',(-0.5,0.,0.866025403784439));
#9090=DIRECTION('',(0.5,0.,-0.866025403784439));
#9091=DIRECTION('',(-0.5,0.,0.866025403784439));
#9092=DIRECTION('center_axis',(0.,1.,0.));
#9093=DIRECTION('ref_axis',(1.,0.,0.));
#9094=DIRECTION('center_axis',(0.,-1.,0.));
#9095=DIRECTION('ref_axis',(0.,0.,-1.));
#11237=CARTESIAN_POINT('',(0.,0.,0.));
#11238=CARTESIAN_POINT('Origin',(0.3,0.4,0.));
#11239=CARTESIAN_POINT('',(-0.3,0.4,-3.67394039744206E-17));
#11240=CARTESIAN_POINT('Origin',(0.,0.4,0.));
#11241=CARTESIAN_POINT('Origin',(0.,0.375,0.));
#11242=CARTESIAN_POINT('',(-0.35,0.35,-4.28626379701573E-17));
#11243=CARTESIAN_POINT('Origin',(0.,0.35,0.));
#11244=CARTESIAN_POINT('',(-0.325,0.375,-3.9801020972289E-17));
#11245=CARTESIAN_POINT('Origin',(0.,0.19,0.));
#11246=CARTESIAN_POINT('',(-0.35,0.03,-4.28626379701574E-17));
#11247=CARTESIAN_POINT('Origin',(0.,0.03,0.));
#11248=CARTESIAN_POINT('',(-0.35,0.19,-4.28626379701574E-17));
#11249=CARTESIAN_POINT('Origin',(0.,0.0149999999999999,0.));
#11250=CARTESIAN_POINT('',(-0.32,-3.29597460435593E-17,-3.91886975727153E-17));
#11251=CARTESIAN_POINT('Origin',(0.,0.,0.));
#11252=CARTESIAN_POINT('',(-0.335,0.0149999999999999,-4.10256677714363E-17));
#11253=CARTESIAN_POINT('Origin',(0.22,0.,0.));
#11254=CARTESIAN_POINT('',(-0.22,-6.93889390390723E-18,-2.69422295812418E-17));
#11255=CARTESIAN_POINT('Origin',(0.,0.,0.));
#11256=CARTESIAN_POINT('Origin',(0.,-0.02,0.));
#11257=CARTESIAN_POINT('',(-0.1954,-0.0492,2.39295984553393E-17));
#11258=CARTESIAN_POINT('Origin',(0.,-0.0492,0.));
#11259=CARTESIAN_POINT('',(-0.21,-0.02,-2.57175827820944E-17));
#11260=CARTESIAN_POINT('Origin',(0.,-0.8,0.));
#11261=CARTESIAN_POINT('',(-0.1954,-1.5646,2.39295984553393E-17));
#11262=CARTESIAN_POINT('Origin',(0.,-1.5646,0.));
#11263=CARTESIAN_POINT('',(-0.1954,-0.8,-2.39295984553393E-17));
#11264=CARTESIAN_POINT('Origin',(0.,-1.58,0.));
#11265=CARTESIAN_POINT('',(-0.16,-1.6,-1.95943487863577E-17));
#11266=CARTESIAN_POINT('Origin',(0.,-1.6,0.));
#11267=CARTESIAN_POINT('',(-0.18,-1.58,-2.20436423846524E-17));
#11268=CARTESIAN_POINT('Origin',(0.,-1.6,0.));
#11269=CARTESIAN_POINT('Origin',(0.0866025403784439,-0.4,-0.15));
#11270=CARTESIAN_POINT('',(0.173205080756888,-0.4,0.));
#11271=CARTESIAN_POINT('',(0.0866025403784439,-0.4,-0.15));
#11272=CARTESIAN_POINT('',(0.173205080756888,-0.4,0.));
#11273=CARTESIAN_POINT('',(0.0866025403784439,-0.64,-0.15));
#11274=CARTESIAN_POINT('',(0.0866025403784439,-0.4,-0.15));
#11275=CARTESIAN_POINT('',(0.173205080756888,-0.64,0.));
#11276=CARTESIAN_POINT('',(0.173205080756888,-0.64,0.));
#11277=CARTESIAN_POINT('',(0.173205080756888,-0.4,0.));
#11278=CARTESIAN_POINT('Origin',(-0.0866025403784438,-0.4,-0.15));
#11279=CARTESIAN_POINT('',(-0.0866025403784438,-0.4,-0.15));
#11280=CARTESIAN_POINT('',(0.0866025403784439,-0.4,-0.15));
#11281=CARTESIAN_POINT('',(-0.0866025403784438,-0.64,-0.15));
#11282=CARTESIAN_POINT('',(-0.0866025403784438,-0.4,-0.15));
#11283=CARTESIAN_POINT('',(0.0866025403784439,-0.64,-0.15));
#11284=CARTESIAN_POINT('Origin',(-0.173205080756888,-0.4,-2.77555756156289E-17));
#11285=CARTESIAN_POINT('',(-0.173205080756888,-0.4,-2.12115047744981E-17));
#11286=CARTESIAN_POINT('',(-0.0866025403784438,-0.4,-0.15));
#11287=CARTESIAN_POINT('',(-0.173205080756888,-0.64,-2.77555756156289E-17));
#11288=CARTESIAN_POINT('',(-0.173205080756888,-0.4,-2.12115047744981E-17));
#11289=CARTESIAN_POINT('',(-0.0866025403784438,-0.64,-0.15));
#11290=CARTESIAN_POINT('Origin',(-0.0866025403784439,-0.4,0.15));
#11291=CARTESIAN_POINT('',(-0.0866025403784439,-0.4,0.15));
#11292=CARTESIAN_POINT('',(-0.173205080756888,-0.4,-2.12115047744981E-17));
#11293=CARTESIAN_POINT('',(-0.0866025403784439,-0.64,0.15));
#11294=CARTESIAN_POINT('',(-0.0866025403784439,-0.4,0.15));
#11295=CARTESIAN_POINT('',(-0.173205080756888,-0.64,-2.12115047744981E-17));
#11296=CARTESIAN_POINT('Origin',(0.0866025403784439,-0.4,0.15));
#11297=CARTESIAN_POINT('',(0.0866025403784439,-0.4,0.15));
#11298=CARTESIAN_POINT('',(-0.0866025403784439,-0.4,0.15));
#11299=CARTESIAN_POINT('',(0.0866025403784439,-0.64,0.15));
#11300=CARTESIAN_POINT('',(0.0866025403784439,-0.4,0.15));
#11301=CARTESIAN_POINT('',(-0.0866025403784439,-0.64,0.15));
#11302=CARTESIAN_POINT('Origin',(0.173205080756888,-0.4,0.));
#11303=CARTESIAN_POINT('',(0.0866025403784439,-0.4,0.15));
#11304=CARTESIAN_POINT('',(0.0866025403784439,-0.64,0.15));
#11305=CARTESIAN_POINT('Origin',(0.,-0.4,-2.77555756156289E-17));
#11306=CARTESIAN_POINT('Origin',(0.,-0.64,-2.77555756156289E-17));
#11392=UNCERTAINTY_MEASURE_WITH_UNIT(LENGTH_MEASURE(0.001),#11433,
'DISTANCE_ACCURACY_VALUE',
'Maximum model space distance between geometric entities at asserted c
onnectivities');
#11393=UNCERTAINTY_MEASURE_WITH_UNIT(LENGTH_MEASURE(0.001),#11433,
'DISTANCE_ACCURACY_VALUE',
'Maximum model space distance between geometric entities at asserted c
onnectivities');
#11431=(
GEOMETRIC_REPRESENTATION_CONTEXT(3)
GLOBAL_UNCERTAINTY_ASSIGNED_CONTEXT((#11392))
GLOBAL_UNIT_ASSIGNED_CONTEXT((#11433,#11435,#11436))
REPRESENTATION_CONTEXT('','3D')
);
#11432=(
GEOMETRIC_REPRESENTATION_CONTEXT(3)
GLOBAL_UNCERTAINTY_ASSIGNED_CONTEXT((#11393))
GLOBAL_UNIT_ASSIGNED_CONTEXT((#11433,#11435,#11436))
REPRESENTATION_CONTEXT('','3D')
);
#11433=(
LENGTH_UNIT()
NAMED_UNIT(*)
SI_UNIT(.CENTI.,.METRE.)
);
#11435=(
NAMED_UNIT(*)
PLANE_ANGLE_UNIT()
SI_UNIT($,.RADIAN.)
);
#11436=(
NAMED_UNIT(*)
SI_UNIT($,.STERADIAN.)
SOLID_ANGLE_UNIT()
);
#11474=SHAPE_DEFINITION_REPRESENTATION(#11514,#11600);
#11514=PRODUCT_DEFINITION_SHAPE('',$,#11639);
#11600=SHAPE_REPRESENTATION('',(#7185),#11431);
#11601=PRODUCT_DEFINITION_CONTEXT('part definition',#11717,'design');
#11639=PRODUCT_DEFINITION('Cap Screw - M4x16',
'Cap Screw - M4x16',#11677,#11601);
#11677=PRODUCT_DEFINITION_FORMATION('',$,#11756);
#11717=APPLICATION_CONTEXT(
'Core Data for Automotive Mechanical Design Process');
#11718=PRODUCT_CONTEXT('part definition',#11717,'mechanical');
#11756=PRODUCT('Cap Screw - M4x16','Cap Screw - M4x16',
'Cap Screw - M4x16',(#11718));
#11820=COLOUR_RGB('Black',0.12,0.14,0.17);
#11821=FILL_AREA_STYLE_COLOUR('',#11820);
#11822=FILL_AREA_STYLE('',(#11821));
#11823=SURFACE_STYLE_FILL_AREA(#11822);
#11824=SURFACE_SIDE_STYLE('',(#11823));
#11825=SURFACE_STYLE_USAGE(.BOTH.,#11824);
#11826=PRESENTATION_STYLE_ASSIGNMENT((#11825));
ENDSEC;
END-ISO-10303-21;
